ISO-10303-21;
HEADER;
/* Generated by software containing ST-Developer
 * from STEP Tools, Inc. (www.steptools.com) 
 */

FILE_DESCRIPTION(
/* description */ ('Indexing fixture plate with plunger'),
/* implementation_level */ '2;1');

FILE_NAME(
/* name */ 'Bonded foot (3).step',
/* time_stamp */ '2026-10-28T03:23:41-07:00',
/* author */ (''),
/* organization */ (''),
/* preprocessor_version */ 'ST-DEVELOPER v20.2',
/* originating_system */ 'Autodesk Translation Framework v15.17.0.0',
/* authorisation */ '');

FILE_SCHEMA (('AUTOMOTIVE_DESIGN { 1 0 10303 214 3 1 1 }'));
ENDSEC;

DATA;
#10=MECHANICAL_DESIGN_GEOMETRIC_PRESENTATION_REPRESENTATION('',(#321),#10020);
#267=SHAPE_REPRESENTATION_RELATIONSHIP('SRR','None',#10141,#294);
#294=ADVANCED_BREP_SHAPE_REPRESENTATION('',(#357),#9994);
#321=STYLED_ITEM('',(#10382),#357);
#357=MANIFOLD_SOLID_BREP('Body1',#4575);
#549=PLANE('',#4959);
#550=PLANE('',#4960);
#692=FACE_OUTER_BOUND('',#992,.T.);
#693=FACE_OUTER_BOUND('',#993,.T.);
#694=FACE_OUTER_BOUND('',#994,.T.);
#992=EDGE_LOOP('',(#3147,#3148,#3149,#3150));
#993=EDGE_LOOP('',(#3151));
#994=EDGE_LOOP('',(#3152));
#1414=LINE('',#7228,#1634);
#1634=VECTOR('',#5697,1.);
#1852=CIRCLE('',#4957,1.);
#1853=CIRCLE('',#4958,1.);
#2163=VERTEX_POINT('',#7225);
#2164=VERTEX_POINT('',#7227);
#2553=EDGE_CURVE('',#2163,#2163,#1852,.T.);
#2554=EDGE_CURVE('',#2163,#2164,#1414,.T.);
#2555=EDGE_CURVE('',#2164,#2164,#1853,.T.);
#3147=ORIENTED_EDGE('',*,*,#2553,.F.);
#3148=ORIENTED_EDGE('',*,*,#2554,.T.);
#3149=ORIENTED_EDGE('',*,*,#2555,.T.);
#3150=ORIENTED_EDGE('',*,*,#2554,.F.);
#3151=ORIENTED_EDGE('',*,*,#2553,.T.);
#3152=ORIENTED_EDGE('',*,*,#2555,.F.);
#4177=CYLINDRICAL_SURFACE('',#4956,1.);
#4307=ADVANCED_FACE('',(#692),#4177,.T.);
#4308=ADVANCED_FACE('',(#693),#549,.T.);
#4309=ADVANCED_FACE('',(#694),#550,.F.);
#4575=CLOSED_SHELL('',(#4307,#4308,#4309));
#4955=AXIS2_PLACEMENT_3D('',#7223,#5691,#5692);
#4956=AXIS2_PLACEMENT_3D('',#7224,#5693,#5694);
#4957=AXIS2_PLACEMENT_3D('',#7226,#5695,#5696);
#4958=AXIS2_PLACEMENT_3D('',#7229,#5698,#5699);
#4959=AXIS2_PLACEMENT_3D('',#7230,#5700,#5701);
#4960=AXIS2_PLACEMENT_3D('',#7231,#5702,#5703);
#5691=DIRECTION('axis',(0.,0.,1.));
#5692=DIRECTION('refdir',(1.,0.,0.));
#5693=DIRECTION('center_axis',(0.,0.,1.));
#5694=DIRECTION('ref_axis',(1.,0.,0.));
#5695=DIRECTION('center_axis',(0.,0.,1.));
#5696=DIRECTION('ref_axis',(1.,0.,0.));
#5697=DIRECTION('',(0.,0.,-1.));
#5698=DIRECTION('center_axis',(0.,0.,1.));
#5699=DIRECTION('ref_axis',(1.,0.,0.));
#5700=DIRECTION('center_axis',(0.,0.,1.));
#5701=DIRECTION('ref_axis',(1.,0.,0.));
#5702=DIRECTION('center_axis',(0.,0.,1.));
#5703=DIRECTION('ref_axis',(1.,0.,0.));
#7223=CARTESIAN_POINT('',(0.,0.,0.));
#7224=CARTESIAN_POINT('Origin',(9.5,9.5,-3.5));
#7225=CARTESIAN_POINT('',(8.5,9.5,-1.));
#7226=CARTESIAN_POINT('Origin',(9.5,9.5,-1.));
#7227=CARTESIAN_POINT('',(8.5,9.5,-3.5));
#7228=CARTESIAN_POINT('',(8.5,9.5,-3.5));
#7229=CARTESIAN_POINT('Origin',(9.5,9.5,-3.5));
#7230=CARTESIAN_POINT('Origin',(9.5,9.5,-1.));
#7231=CARTESIAN_POINT('Origin',(9.5,9.5,-3.5));
#9961=UNCERTAINTY_MEASURE_WITH_UNIT(LENGTH_MEASURE(0.001),#10021,
'DISTANCE_ACCURACY_VALUE',
'Maximum model space distance between geometric entities at asserted c
onnectivities');
#9987=UNCERTAINTY_MEASURE_WITH_UNIT(LENGTH_MEASURE(0.001),#10021,
'DISTANCE_ACCURACY_VALUE',
'Maximum model space distance between geometric entities at asserted c
onnectivities');
#9994=(
GEOMETRIC_REPRESENTATION_CONTEXT(3)
GLOBAL_UNCERTAINTY_ASSIGNED_CONTEXT((#9961))
GLOBAL_UNIT_ASSIGNED_CONTEXT((#10021,#10023,#10024))
REPRESENTATION_CONTEXT('','3D')
);
#10020=(
GEOMETRIC_REPRESENTATION_CONTEXT(3)
GLOBAL_UNCERTAINTY_ASSIGNED_CONTEXT((#9987))
GLOBAL_UNIT_ASSIGNED_CONTEXT((#10021,#10023,#10024))
REPRESENTATION_CONTEXT('','3D')
);
#10021=(
LENGTH_UNIT()
NAMED_UNIT(*)
SI_UNIT(.CENTI.,.METRE.)
);
#10023=(
NAMED_UNIT(*)
PLANE_ANGLE_UNIT()
SI_UNIT($,.RADIAN.)
);
#10024=(
NAMED_UNIT(*)
SI_UNIT($,.STERADIAN.)
SOLID_ANGLE_UNIT()
);
#10031=SHAPE_DEFINITION_REPRESENTATION(#10063,#10141);
#10063=PRODUCT_DEFINITION_SHAPE('',$,#10174);
#10141=SHAPE_REPRESENTATION('',(#4955),#9994);
#10167=PRODUCT_DEFINITION_CONTEXT('part definition',#10265,'design');
#10174=PRODUCT_DEFINITION('Bonded foot (3)','Bonded foot (3)',#10206,#10167);
#10206=PRODUCT_DEFINITION_FORMATION('',$,#10273);
#10265=APPLICATION_CONTEXT(
'Core Data for Automotive Mechanical Design Process');
#10266=PRODUCT_CONTEXT('part definition',#10265,'mechanical');
#10273=PRODUCT('Bonded foot (3)','Bonded foot (3)','Bonded foot (3)',(#10266));
#10376=COLOUR_RGB('Off White',0.89,0.88,0.83);
#10377=FILL_AREA_STYLE_COLOUR('',#10376);
#10378=FILL_AREA_STYLE('',(#10377));
#10379=SURFACE_STYLE_FILL_AREA(#10378);
#10380=SURFACE_SIDE_STYLE('',(#10379));
#10381=SURFACE_STYLE_USAGE(.BOTH.,#10380);
#10382=PRESENTATION_STYLE_ASSIGNMENT((#10381));
ENDSEC;
END-ISO-10303-21;
